ISO-10303-21;
HEADER;
/* Generated by software containing ST-Developer
 * from STEP Tools, Inc. (www.steptools.com) 
 */

FILE_DESCRIPTION(
/* description */ ('Shaft runout checking stand'),
/* implementation_level */ '2;1');

FILE_NAME(
/* name */ 'Inner race spacer (3).step',
/* time_stamp */ '2026-11-02T21:12:33-08:00',
/* author */ (''),
/* organization */ (''),
/* preprocessor_version */ 'ST-DEVELOPER v20.2',
/* originating_system */ 'Autodesk Translation Framework v15.17.0.0',
/* authorisation */ '');

FILE_SCHEMA (('AUTOMOTIVE_DESIGN { 1 0 10303 214 3 1 1 }'));
ENDSEC;

DATA;
#10=MECHANICAL_DESIGN_GEOMETRIC_PRESENTATION_REPRESENTATION('',(#475),#11748);
#389=SHAPE_REPRESENTATION_RELATIONSHIP('SRR','None',#11938,#432);
#432=ADVANCED_BREP_SHAPE_REPRESENTATION('',(#526),#11714);
#475=STYLED_ITEM('',(#12170),#526);
#526=MANIFOLD_SOLID_BREP('Body1',#6218);
#609=FACE_BOUND('',#1592,.T.);
#610=FACE_BOUND('',#1594,.T.);
#742=CIRCLE('',#6957,0.505);
#743=CIRCLE('',#6958,0.505);
#744=CIRCLE('',#6960,0.7);
#745=CIRCLE('',#6961,0.7);
#971=CYLINDRICAL_SURFACE('',#6956,0.505);
#972=CYLINDRICAL_SURFACE('',#6959,0.7);
#1174=FACE_OUTER_BOUND('',#1589,.T.);
#1175=FACE_OUTER_BOUND('',#1590,.T.);
#1176=FACE_OUTER_BOUND('',#1591,.T.);
#1177=FACE_OUTER_BOUND('',#1593,.T.);
#1589=EDGE_LOOP('',(#4740,#4741,#4742,#4743));
#1590=EDGE_LOOP('',(#4744,#4745,#4746,#4747));
#1591=EDGE_LOOP('',(#4748));
#1592=EDGE_LOOP('',(#4749));
#1593=EDGE_LOOP('',(#4750));
#1594=EDGE_LOOP('',(#4751));
#2140=LINE('',#10173,#2607);
#2141=LINE('',#10179,#2608);
#2607=VECTOR('',#8195,0.505);
#2608=VECTOR('',#8202,0.7);
#3036=VERTEX_POINT('',#10170);
#3037=VERTEX_POINT('',#10172);
#3038=VERTEX_POINT('',#10176);
#3039=VERTEX_POINT('',#10178);
#3656=EDGE_CURVE('',#3036,#3036,#742,.T.);
#3657=EDGE_CURVE('',#3036,#3037,#2140,.T.);
#3658=EDGE_CURVE('',#3037,#3037,#743,.T.);
#3659=EDGE_CURVE('',#3038,#3038,#744,.T.);
#3660=EDGE_CURVE('',#3038,#3039,#2141,.T.);
#3661=EDGE_CURVE('',#3039,#3039,#745,.T.);
#4740=ORIENTED_EDGE('',*,*,#3656,.F.);
#4741=ORIENTED_EDGE('',*,*,#3657,.T.);
#4742=ORIENTED_EDGE('',*,*,#3658,.T.);
#4743=ORIENTED_EDGE('',*,*,#3657,.F.);
#4744=ORIENTED_EDGE('',*,*,#3659,.F.);
#4745=ORIENTED_EDGE('',*,*,#3660,.T.);
#4746=ORIENTED_EDGE('',*,*,#3661,.T.);
#4747=ORIENTED_EDGE('',*,*,#3660,.F.);
#4748=ORIENTED_EDGE('',*,*,#3659,.T.);
#4749=ORIENTED_EDGE('',*,*,#3656,.T.);
#4750=ORIENTED_EDGE('',*,*,#3661,.F.);
#4751=ORIENTED_EDGE('',*,*,#3658,.F.);
#5706=PLANE('',#6962);
#5707=PLANE('',#6963);
#5974=ADVANCED_FACE('',(#1174),#971,.F.);
#5975=ADVANCED_FACE('',(#1175),#972,.T.);
#5976=ADVANCED_FACE('',(#1176,#609),#5706,.T.);
#5977=ADVANCED_FACE('',(#1177,#610),#5707,.F.);
#6218=CLOSED_SHELL('',(#5974,#5975,#5976,#5977));
#6955=AXIS2_PLACEMENT_3D('',#10168,#8189,#8190);
#6956=AXIS2_PLACEMENT_3D('',#10169,#8191,#8192);
#6957=AXIS2_PLACEMENT_3D('',#10171,#8193,#8194);
#6958=AXIS2_PLACEMENT_3D('',#10174,#8196,#8197);
#6959=AXIS2_PLACEMENT_3D('',#10175,#8198,#8199);
#6960=AXIS2_PLACEMENT_3D('',#10177,#8200,#8201);
#6961=AXIS2_PLACEMENT_3D('',#10180,#8203,#8204);
#6962=AXIS2_PLACEMENT_3D('',#10181,#8205,#8206);
#6963=AXIS2_PLACEMENT_3D('',#10182,#8207,#8208);
#8189=DIRECTION('axis',(0.,0.,1.));
#8190=DIRECTION('refdir',(1.,0.,0.));
#8191=DIRECTION('center_axis',(0.,1.,0.));
#8192=DIRECTION('ref_axis',(1.,0.,0.));
#8193=DIRECTION('center_axis',(0.,-1.,0.));
#8194=DIRECTION('ref_axis',(1.,0.,0.));
#8195=DIRECTION('',(0.,-1.,0.));
#8196=DIRECTION('center_axis',(0.,-1.,0.));
#8197=DIRECTION('ref_axis',(1.,0.,0.));
#8198=DIRECTION('center_axis',(0.,1.,0.));
#8199=DIRECTION('ref_axis',(1.,0.,0.));
#8200=DIRECTION('center_axis',(0.,1.,0.));
#8201=DIRECTION('ref_axis',(1.,0.,0.));
#8202=DIRECTION('',(0.,-1.,0.));
#8203=DIRECTION('center_axis',(0.,1.,0.));
#8204=DIRECTION('ref_axis',(1.,0.,0.));
#8205=DIRECTION('center_axis',(0.,1.,0.));
#8206=DIRECTION('ref_axis',(1.,0.,0.));
#8207=DIRECTION('center_axis',(0.,1.,0.));
#8208=DIRECTION('ref_axis',(1.,0.,0.));
#10168=CARTESIAN_POINT('',(0.,0.,0.));
#10169=CARTESIAN_POINT('Origin',(2.,-9.55,5.));
#10170=CARTESIAN_POINT('',(1.495,-9.2,5.));
#10171=CARTESIAN_POINT('Origin',(2.,-9.2,5.));
#10172=CARTESIAN_POINT('',(1.495,-9.55,5.));
#10173=CARTESIAN_POINT('',(1.495,-9.55,5.));
#10174=CARTESIAN_POINT('Origin',(2.,-9.55,5.));
#10175=CARTESIAN_POINT('Origin',(2.,-9.55,5.));
#10176=CARTESIAN_POINT('',(1.3,-9.2,5.));
#10177=CARTESIAN_POINT('Origin',(2.,-9.2,5.));
#10178=CARTESIAN_POINT('',(1.3,-9.55,5.));
#10179=CARTESIAN_POINT('',(1.3,-9.55,5.));
#10180=CARTESIAN_POINT('Origin',(2.,-9.55,5.));
#10181=CARTESIAN_POINT('Origin',(2.,-9.2,5.));
#10182=CARTESIAN_POINT('Origin',(2.,-9.55,5.));
#11665=UNCERTAINTY_MEASURE_WITH_UNIT(LENGTH_MEASURE(0.001),#11749,
'DISTANCE_ACCURACY_VALUE',
'Maximum model space distance between geometric entities at asserted c
onnectivities');
#11699=UNCERTAINTY_MEASURE_WITH_UNIT(LENGTH_MEASURE(0.001),#11749,
'DISTANCE_ACCURACY_VALUE',
'Maximum model space distance between geometric entities at asserted c
onnectivities');
#11714=(
GEOMETRIC_REPRESENTATION_CONTEXT(3)
GLOBAL_UNCERTAINTY_ASSIGNED_CONTEXT((#11665))
GLOBAL_UNIT_ASSIGNED_CONTEXT((#11749,#11751,#11752))
REPRESENTATION_CONTEXT('','3D')
);
#11748=(
GEOMETRIC_REPRESENTATION_CONTEXT(3)
GLOBAL_UNCERTAINTY_ASSIGNED_CONTEXT((#11699))
GLOBAL_UNIT_ASSIGNED_CONTEXT((#11749,#11751,#11752))
REPRESENTATION_CONTEXT('','3D')
);
#11749=(
LENGTH_UNIT()
NAMED_UNIT(*)
SI_UNIT(.CENTI.,.METRE.)
);
#11751=(
NAMED_UNIT(*)
PLANE_ANGLE_UNIT()
SI_UNIT($,.RADIAN.)
);
#11752=(
NAMED_UNIT(*)
SI_UNIT($,.STERADIAN.)
SOLID_ANGLE_UNIT()
);
#11767=SHAPE_DEFINITION_REPRESENTATION(#11815,#11938);
#11815=PRODUCT_DEFINITION_SHAPE('',$,#11987);
#11938=SHAPE_REPRESENTATION('',(#6955),#11714);
#11972=PRODUCT_DEFINITION_CONTEXT('part definition',#12118,'design');
#11987=PRODUCT_DEFINITION('Inner race spacer_2','Inner race spacer (3)',
#12035,#11972);
#12035=PRODUCT_DEFINITION_FORMATION('',$,#12134);
#12118=APPLICATION_CONTEXT(
'Core Data for Automotive Mechanical Design Process');
#12119=PRODUCT_CONTEXT('part definition',#12118,'mechanical');
#12134=PRODUCT('Inner race spacer_2','Inner race spacer (3)',
'Inner race spacer',(#12119));
#12170=PRESENTATION_STYLE_ASSIGNMENT((#12175));
#12175=SURFACE_STYLE_USAGE(.BOTH.,#12180);
#12180=SURFACE_SIDE_STYLE('',(#12185));
#12185=SURFACE_STYLE_FILL_AREA(#12190);
#12190=FILL_AREA_STYLE('CAD Library Painted - Steel gray',(#12195));
#12195=FILL_AREA_STYLE_COLOUR('CAD Library Painted - Steel gray',#12200);
#12200=COLOUR_RGB('CAD Library Painted - Steel gray',0.592156862745098,
0.631372549019608,0.67843137254902);
ENDSEC;
END-ISO-10303-21;
